ISO-10303-21;
HEADER;
/* Generated by software containing ST-Developer
 * from STEP Tools, Inc. (www.steptools.com) 
 */

FILE_DESCRIPTION(
/* description */ ('PAT-041'),
/* implementation_level */ '2;1');

FILE_NAME(
/* name */ 'Hex Bolt - M8x40.step',
/* time_stamp */ '2026-10-28T22:21:24-07:00',
/* author */ (''),
/* organization */ (''),
/* preprocessor_version */ 'ST-DEVELOPER v20.2',
/* originating_system */ 'Autodesk Translation Framework v15.17.0.0',
/* authorisation */ '');

FILE_SCHEMA (('AUTOMOTIVE_DESIGN { 1 0 10303 214 3 1 1 }'));
ENDSEC;

DATA;
#10=MECHANICAL_DESIGN_GEOMETRIC_PRESENTATION_REPRESENTATION('',(#216),#2507);
#167=(
BOUNDED_CURVE()
B_SPLINE_CURVE(2,(#2305,#2306,#2307),.UNSPECIFIED.,.F.,.F.)
B_SPLINE_CURVE_WITH_KNOTS((3,3),(0.14973948338295,0.97160236658079),
 .UNSPECIFIED.)
CURVE()
GEOMETRIC_REPRESENTATION_ITEM()
RATIONAL_B_SPLINE_CURVE((1.07140024848292,1.23714644374248,1.07140024848292))
REPRESENTATION_ITEM('')
);
#168=(
BOUNDED_CURVE()
B_SPLINE_CURVE(2,(#2309,#2310,#2311),.UNSPECIFIED.,.F.,.F.)
B_SPLINE_CURVE_WITH_KNOTS((3,3),(0.14973948338295,0.97160236658079),
 .UNSPECIFIED.)
CURVE()
GEOMETRIC_REPRESENTATION_ITEM()
RATIONAL_B_SPLINE_CURVE((1.07140024848292,1.23714644374248,1.07140024848292))
REPRESENTATION_ITEM('')
);
#169=(
BOUNDED_CURVE()
B_SPLINE_CURVE(2,(#2313,#2314,#2315),.UNSPECIFIED.,.F.,.F.)
B_SPLINE_CURVE_WITH_KNOTS((3,3),(0.14973948338295,0.97160236658079),
 .UNSPECIFIED.)
CURVE()
GEOMETRIC_REPRESENTATION_ITEM()
RATIONAL_B_SPLINE_CURVE((1.07140024848292,1.23714644374248,1.07140024848292))
REPRESENTATION_ITEM('')
);
#170=(
BOUNDED_CURVE()
B_SPLINE_CURVE(2,(#2317,#2318,#2319),.UNSPECIFIED.,.F.,.F.)
B_SPLINE_CURVE_WITH_KNOTS((3,3),(0.149739483382949,0.971602366580789),
 .UNSPECIFIED.)
CURVE()
GEOMETRIC_REPRESENTATION_ITEM()
RATIONAL_B_SPLINE_CURVE((1.07140024848292,1.23714644374248,1.07140024848292))
REPRESENTATION_ITEM('')
);
#171=(
BOUNDED_CURVE()
B_SPLINE_CURVE(2,(#2321,#2322,#2323),.UNSPECIFIED.,.F.,.F.)
B_SPLINE_CURVE_WITH_KNOTS((3,3),(0.14973948338295,0.971602366580789),
 .UNSPECIFIED.)
CURVE()
GEOMETRIC_REPRESENTATION_ITEM()
RATIONAL_B_SPLINE_CURVE((1.07140024848292,1.23714644374248,1.07140024848292))
REPRESENTATION_ITEM('')
);
#172=(
BOUNDED_CURVE()
B_SPLINE_CURVE(2,(#2324,#2325,#2326),.UNSPECIFIED.,.F.,.F.)
B_SPLINE_CURVE_WITH_KNOTS((3,3),(0.14973948338295,0.97160236658079),
 .UNSPECIFIED.)
CURVE()
GEOMETRIC_REPRESENTATION_ITEM()
RATIONAL_B_SPLINE_CURVE((1.07140024848292,1.23714644374248,1.07140024848292))
REPRESENTATION_ITEM('')
);
#185=CONICAL_SURFACE('',#1566,0.36,0.785398163397451);
#186=CONICAL_SURFACE('',#1569,0.734027674973257,1.0471975511966);
#196=SHAPE_REPRESENTATION_RELATIONSHIP('SRR','None',#2581,#206);
#206=ADVANCED_BREP_SHAPE_REPRESENTATION('',(#226),#2504);
#216=STYLED_ITEM('',(#2701),#226);
#226=MANIFOLD_SOLID_BREP('Body1',#1336);
#275=FACE_BOUND('',#486,.T.);
#294=PLANE('',#1568);
#295=PLANE('',#1571);
#296=PLANE('',#1572);
#297=PLANE('',#1573);
#298=PLANE('',#1574);
#299=PLANE('',#1575);
#300=PLANE('',#1576);
#301=PLANE('',#1577);
#302=PLANE('',#1578);
#357=FACE_OUTER_BOUND('',#474,.T.);
#358=FACE_OUTER_BOUND('',#475,.T.);
#359=FACE_OUTER_BOUND('',#476,.T.);
#360=FACE_OUTER_BOUND('',#477,.T.);
#361=FACE_OUTER_BOUND('',#478,.T.);
#362=FACE_OUTER_BOUND('',#479,.T.);
#363=FACE_OUTER_BOUND('',#480,.T.);
#364=FACE_OUTER_BOUND('',#481,.T.);
#365=FACE_OUTER_BOUND('',#482,.T.);
#366=FACE_OUTER_BOUND('',#483,.T.);
#367=FACE_OUTER_BOUND('',#484,.T.);
#368=FACE_OUTER_BOUND('',#485,.T.);
#474=EDGE_LOOP('',(#1112,#1113,#1114,#1115));
#475=EDGE_LOOP('',(#1116,#1117,#1118,#1119));
#476=EDGE_LOOP('',(#1120));
#477=EDGE_LOOP('',(#1121,#1122,#1123,#1124,#1125,#1126,#1127,#1128,#1129));
#478=EDGE_LOOP('',(#1130,#1131,#1132,#1133));
#479=EDGE_LOOP('',(#1134,#1135,#1136,#1137));
#480=EDGE_LOOP('',(#1138,#1139,#1140,#1141));
#481=EDGE_LOOP('',(#1142,#1143,#1144,#1145));
#482=EDGE_LOOP('',(#1146,#1147,#1148,#1149));
#483=EDGE_LOOP('',(#1150,#1151,#1152,#1153));
#484=EDGE_LOOP('',(#1154));
#485=EDGE_LOOP('',(#1155,#1156,#1157,#1158,#1159,#1160));
#486=EDGE_LOOP('',(#1161));
#536=LINE('',#2292,#592);
#537=LINE('',#2297,#593);
#538=LINE('',#2303,#594);
#539=LINE('',#2329,#595);
#540=LINE('',#2331,#596);
#541=LINE('',#2332,#597);
#542=LINE('',#2335,#598);
#543=LINE('',#2336,#599);
#544=LINE('',#2339,#600);
#545=LINE('',#2340,#601);
#546=LINE('',#2343,#602);
#547=LINE('',#2344,#603);
#548=LINE('',#2347,#604);
#549=LINE('',#2348,#605);
#550=LINE('',#2350,#606);
#592=VECTOR('',#1903,0.4);
#593=VECTOR('',#1910,0.36);
#594=VECTOR('',#1917,0.734027674973257);
#595=VECTOR('',#1920,1.);
#596=VECTOR('',#1921,1.);
#597=VECTOR('',#1922,1.);
#598=VECTOR('',#1925,1.);
#599=VECTOR('',#1926,1.);
#600=VECTOR('',#1929,1.);
#601=VECTOR('',#1930,1.);
#602=VECTOR('',#1933,1.);
#603=VECTOR('',#1934,1.);
#604=VECTOR('',#1937,1.);
#605=VECTOR('',#1938,1.);
#606=VECTOR('',#1941,1.);
#678=CIRCLE('',#1564,0.3933);
#679=CIRCLE('',#1565,0.3933);
#680=CIRCLE('',#1567,0.32);
#681=CIRCLE('',#1570,0.6175);
#750=VERTEX_POINT('',#2289);
#751=VERTEX_POINT('',#2291);
#752=VERTEX_POINT('',#2295);
#753=VERTEX_POINT('',#2300);
#754=VERTEX_POINT('',#2302);
#755=VERTEX_POINT('',#2304);
#756=VERTEX_POINT('',#2308);
#757=VERTEX_POINT('',#2312);
#758=VERTEX_POINT('',#2316);
#759=VERTEX_POINT('',#2320);
#760=VERTEX_POINT('',#2328);
#761=VERTEX_POINT('',#2330);
#762=VERTEX_POINT('',#2334);
#763=VERTEX_POINT('',#2338);
#764=VERTEX_POINT('',#2342);
#765=VERTEX_POINT('',#2346);
#876=EDGE_CURVE('',#750,#750,#678,.F.);
#877=EDGE_CURVE('',#750,#751,#536,.T.);
#878=EDGE_CURVE('',#751,#751,#679,.F.);
#879=EDGE_CURVE('',#752,#752,#680,.T.);
#880=EDGE_CURVE('',#752,#750,#537,.T.);
#881=EDGE_CURVE('',#753,#753,#681,.T.);
#882=EDGE_CURVE('',#753,#754,#538,.T.);
#883=EDGE_CURVE('',#755,#754,#167,.T.);
#884=EDGE_CURVE('',#756,#755,#168,.T.);
#885=EDGE_CURVE('',#757,#756,#169,.T.);
#886=EDGE_CURVE('',#758,#757,#170,.T.);
#887=EDGE_CURVE('',#759,#758,#171,.T.);
#888=EDGE_CURVE('',#754,#759,#172,.T.);
#889=EDGE_CURVE('',#760,#758,#539,.T.);
#890=EDGE_CURVE('',#760,#761,#540,.T.);
#891=EDGE_CURVE('',#761,#759,#541,.T.);
#892=EDGE_CURVE('',#762,#757,#542,.T.);
#893=EDGE_CURVE('',#762,#760,#543,.T.);
#894=EDGE_CURVE('',#763,#756,#544,.T.);
#895=EDGE_CURVE('',#763,#762,#545,.T.);
#896=EDGE_CURVE('',#764,#755,#546,.T.);
#897=EDGE_CURVE('',#764,#763,#547,.T.);
#898=EDGE_CURVE('',#765,#754,#548,.T.);
#899=EDGE_CURVE('',#765,#764,#549,.T.);
#900=EDGE_CURVE('',#761,#765,#550,.T.);
#1112=ORIENTED_EDGE('',*,*,#876,.F.);
#1113=ORIENTED_EDGE('',*,*,#877,.T.);
#1114=ORIENTED_EDGE('',*,*,#878,.F.);
#1115=ORIENTED_EDGE('',*,*,#877,.F.);
#1116=ORIENTED_EDGE('',*,*,#879,.F.);
#1117=ORIENTED_EDGE('',*,*,#880,.T.);
#1118=ORIENTED_EDGE('',*,*,#876,.T.);
#1119=ORIENTED_EDGE('',*,*,#880,.F.);
#1120=ORIENTED_EDGE('',*,*,#879,.T.);
#1121=ORIENTED_EDGE('',*,*,#881,.F.);
#1122=ORIENTED_EDGE('',*,*,#882,.T.);
#1123=ORIENTED_EDGE('',*,*,#883,.F.);
#1124=ORIENTED_EDGE('',*,*,#884,.F.);
#1125=ORIENTED_EDGE('',*,*,#885,.F.);
#1126=ORIENTED_EDGE('',*,*,#886,.F.);
#1127=ORIENTED_EDGE('',*,*,#887,.F.);
#1128=ORIENTED_EDGE('',*,*,#888,.F.);
#1129=ORIENTED_EDGE('',*,*,#882,.F.);
#1130=ORIENTED_EDGE('',*,*,#887,.T.);
#1131=ORIENTED_EDGE('',*,*,#889,.F.);
#1132=ORIENTED_EDGE('',*,*,#890,.T.);
#1133=ORIENTED_EDGE('',*,*,#891,.T.);
#1134=ORIENTED_EDGE('',*,*,#886,.T.);
#1135=ORIENTED_EDGE('',*,*,#892,.F.);
#1136=ORIENTED_EDGE('',*,*,#893,.T.);
#1137=ORIENTED_EDGE('',*,*,#889,.T.);
#1138=ORIENTED_EDGE('',*,*,#885,.T.);
#1139=ORIENTED_EDGE('',*,*,#894,.F.);
#1140=ORIENTED_EDGE('',*,*,#895,.T.);
#1141=ORIENTED_EDGE('',*,*,#892,.T.);
#1142=ORIENTED_EDGE('',*,*,#884,.T.);
#1143=ORIENTED_EDGE('',*,*,#896,.F.);
#1144=ORIENTED_EDGE('',*,*,#897,.T.);
#1145=ORIENTED_EDGE('',*,*,#894,.T.);
#1146=ORIENTED_EDGE('',*,*,#883,.T.);
#1147=ORIENTED_EDGE('',*,*,#898,.F.);
#1148=ORIENTED_EDGE('',*,*,#899,.T.);
#1149=ORIENTED_EDGE('',*,*,#896,.T.);
#1150=ORIENTED_EDGE('',*,*,#888,.T.);
#1151=ORIENTED_EDGE('',*,*,#891,.F.);
#1152=ORIENTED_EDGE('',*,*,#900,.T.);
#1153=ORIENTED_EDGE('',*,*,#898,.T.);
#1154=ORIENTED_EDGE('',*,*,#881,.T.);
#1155=ORIENTED_EDGE('',*,*,#895,.F.);
#1156=ORIENTED_EDGE('',*,*,#897,.F.);
#1157=ORIENTED_EDGE('',*,*,#899,.F.);
#1158=ORIENTED_EDGE('',*,*,#900,.F.);
#1159=ORIENTED_EDGE('',*,*,#890,.F.);
#1160=ORIENTED_EDGE('',*,*,#893,.F.);
#1161=ORIENTED_EDGE('',*,*,#878,.T.);
#1254=CYLINDRICAL_SURFACE('',#1563,0.3933);
#1302=ADVANCED_FACE('',(#357),#1254,.T.);
#1303=ADVANCED_FACE('',(#358),#185,.T.);
#1304=ADVANCED_FACE('',(#359),#294,.T.);
#1305=ADVANCED_FACE('',(#360),#186,.T.);
#1306=ADVANCED_FACE('',(#361),#295,.T.);
#1307=ADVANCED_FACE('',(#362),#296,.T.);
#1308=ADVANCED_FACE('',(#363),#297,.T.);
#1309=ADVANCED_FACE('',(#364),#298,.T.);
#1310=ADVANCED_FACE('',(#365),#299,.T.);
#1311=ADVANCED_FACE('',(#366),#300,.T.);
#1312=ADVANCED_FACE('',(#367),#301,.T.);
#1313=ADVANCED_FACE('',(#368,#275),#302,.F.);
#1336=CLOSED_SHELL('',(#1302,#1303,#1304,#1305,#1306,#1307,#1308,#1309,
#1310,#1311,#1312,#1313));
#1562=AXIS2_PLACEMENT_3D('',#2287,#1897,#1898);
#1563=AXIS2_PLACEMENT_3D('',#2288,#1899,#1900);
#1564=AXIS2_PLACEMENT_3D('',#2290,#1901,#1902);
#1565=AXIS2_PLACEMENT_3D('',#2293,#1904,#1905);
#1566=AXIS2_PLACEMENT_3D('',#2294,#1906,#1907);
#1567=AXIS2_PLACEMENT_3D('',#2296,#1908,#1909);
#1568=AXIS2_PLACEMENT_3D('',#2298,#1911,#1912);
#1569=AXIS2_PLACEMENT_3D('',#2299,#1913,#1914);
#1570=AXIS2_PLACEMENT_3D('',#2301,#1915,#1916);
#1571=AXIS2_PLACEMENT_3D('',#2327,#1918,#1919);
#1572=AXIS2_PLACEMENT_3D('',#2333,#1923,#1924);
#1573=AXIS2_PLACEMENT_3D('',#2337,#1927,#1928);
#1574=AXIS2_PLACEMENT_3D('',#2341,#1931,#1932);
#1575=AXIS2_PLACEMENT_3D('',#2345,#1935,#1936);
#1576=AXIS2_PLACEMENT_3D('',#2349,#1939,#1940);
#1577=AXIS2_PLACEMENT_3D('',#2351,#1942,#1943);
#1578=AXIS2_PLACEMENT_3D('',#2352,#1944,#1945);
#1897=DIRECTION('axis',(0.,0.,1.));
#1898=DIRECTION('refdir',(1.,0.,0.));
#1899=DIRECTION('center_axis',(0.,-1.,0.));
#1900=DIRECTION('ref_axis',(1.,0.,0.));
#1901=DIRECTION('center_axis',(0.,1.,0.));
#1902=DIRECTION('ref_axis',(1.,0.,0.));
#1903=DIRECTION('',(0.,1.,0.));
#1904=DIRECTION('center_axis',(0.,-1.,0.));
#1905=DIRECTION('ref_axis',(1.,0.,0.));
#1906=DIRECTION('center_axis',(0.,1.,0.));
#1907=DIRECTION('ref_axis',(1.,0.,0.));
#1908=DIRECTION('center_axis',(0.,-1.,0.));
#1909=DIRECTION('ref_axis',(1.,0.,0.));
#1910=DIRECTION('',(-0.707106781186549,0.707106781186546,-8.65956056235496E-17));
#1911=DIRECTION('center_axis',(0.,-1.,0.));
#1912=DIRECTION('ref_axis',(0.,0.,-1.));
#1913=DIRECTION('center_axis',(0.,-1.,0.));
#1914=DIRECTION('ref_axis',(1.,0.,0.));
#1915=DIRECTION('center_axis',(0.,1.,0.));
#1916=DIRECTION('ref_axis',(1.,0.,0.));
#1917=DIRECTION('',(-0.866025403784439,-0.5,-1.06057523872491E-16));
#1918=DIRECTION('center_axis',(1.4792020664489E-16,0.,-1.));
#1919=DIRECTION('ref_axis',(-1.,0.,-1.4792020664489E-16));
#1920=DIRECTION('',(0.,1.,0.));
#1921=DIRECTION('',(-1.,0.,-1.4792020664489E-16));
#1922=DIRECTION('',(0.,1.,0.));
#1923=DIRECTION('center_axis',(0.866025403784439,0.,-0.5));
#1924=DIRECTION('ref_axis',(-0.5,0.,-0.866025403784439));
#1925=DIRECTION('',(0.,1.,0.));
#1926=DIRECTION('',(-0.5,0.,-0.866025403784439));
#1927=DIRECTION('center_axis',(0.866025403784439,0.,0.5));
#1928=DIRECTION('ref_axis',(0.5,0.,-0.866025403784439));
#1929=DIRECTION('',(0.,1.,0.));
#1930=DIRECTION('',(0.5,0.,-0.866025403784439));
#1931=DIRECTION('center_axis',(-2.95840413289779E-16,0.,1.));
#1932=DIRECTION('ref_axis',(1.,0.,2.95840413289779E-16));
#1933=DIRECTION('',(0.,1.,0.));
#1934=DIRECTION('',(1.,0.,2.95840413289779E-16));
#1935=DIRECTION('center_axis',(-0.866025403784439,0.,0.5));
#1936=DIRECTION('ref_axis',(0.5,0.,0.866025403784439));
#1937=DIRECTION('',(0.,1.,0.));
#1938=DIRECTION('',(0.5,0.,0.866025403784439));
#1939=DIRECTION('center_axis',(-0.866025403784439,0.,-0.5));
#1940=DIRECTION('ref_axis',(-0.5,0.,0.866025403784439));
#1941=DIRECTION('',(-0.5,0.,0.866025403784439));
#1942=DIRECTION('center_axis',(0.,1.,0.));
#1943=DIRECTION('ref_axis',(0.,0.,1.));
#1944=DIRECTION('center_axis',(0.,1.,0.));
#1945=DIRECTION('ref_axis',(1.,0.,0.));
#2287=CARTESIAN_POINT('',(0.,0.,0.));
#2288=CARTESIAN_POINT('Origin',(0.,-1.935,0.));
#2289=CARTESIAN_POINT('',(-0.3933,-3.9267,4.81653586104654E-17));
#2290=CARTESIAN_POINT('Origin',(0.,-3.9267,0.));
#2291=CARTESIAN_POINT('',(-0.3933,0.,-4.81653586104654E-17));
#2292=CARTESIAN_POINT('',(-0.3933,-1.935,-4.81653586104654E-17));
#2293=CARTESIAN_POINT('Origin',(0.,0.,0.));
#2294=CARTESIAN_POINT('Origin',(0.,-3.96,0.));
#2295=CARTESIAN_POINT('',(-0.32,-4.,-3.91886975727153E-17));
#2296=CARTESIAN_POINT('Origin',(0.,-4.,0.));
#2297=CARTESIAN_POINT('',(-0.36,-3.96,-4.40872847693047E-17));
#2298=CARTESIAN_POINT('Origin',(0.,-4.,0.));
#2299=CARTESIAN_POINT('Origin',(0.,0.462722715486149,0.));
#2300=CARTESIAN_POINT('',(-0.6175,0.53,-7.5621939847349E-17));
#2301=CARTESIAN_POINT('Origin',(0.,0.53,0.));
#2302=CARTESIAN_POINT('',(-0.750555349946514,0.453180457891261,-9.19165206894919E-17));
#2303=CARTESIAN_POINT('',(-0.734027674973257,0.462722715486149,-8.98924642641573E-17));
#2304=CARTESIAN_POINT('',(-0.375277674973257,0.453180457891261,0.65));
#2305=CARTESIAN_POINT('Ctrl Pts',(-0.375277674973257,0.45318045789126,0.65));
#2306=CARTESIAN_POINT('Ctrl Pts',(-0.562916512459968,0.561513791224244,
0.324999999999856));
#2307=CARTESIAN_POINT('Ctrl Pts',(-0.750555349946514,0.45318045789126,-9.19165206894919E-17));
#2308=CARTESIAN_POINT('',(0.375277674973257,0.453180457891261,0.65));
#2309=CARTESIAN_POINT('Ctrl Pts',(0.375277674973257,0.453180457891261,0.65));
#2310=CARTESIAN_POINT('Ctrl Pts',(-1.66922031752392E-13,0.561513791224244,
0.65));
#2311=CARTESIAN_POINT('Ctrl Pts',(-0.375277674973257,0.45318045789126,0.65));
#2312=CARTESIAN_POINT('',(0.750555349946514,0.453180457891261,0.));
#2313=CARTESIAN_POINT('Ctrl Pts',(0.750555349946514,0.453180457891261,0.));
#2314=CARTESIAN_POINT('Ctrl Pts',(0.562916512459802,0.561513791224244,0.325000000000144));
#2315=CARTESIAN_POINT('Ctrl Pts',(0.375277674973257,0.45318045789126,0.65));
#2316=CARTESIAN_POINT('',(0.375277674973257,0.453180457891261,-0.65));
#2317=CARTESIAN_POINT('Ctrl Pts',(0.375277674973257,0.45318045789126,-0.65));
#2318=CARTESIAN_POINT('Ctrl Pts',(0.562916512459968,0.561513791224244,-0.324999999999855));
#2319=CARTESIAN_POINT('Ctrl Pts',(0.750555349946514,0.453180457891261,0.));
#2320=CARTESIAN_POINT('',(-0.375277674973257,0.45318045789126,-0.65));
#2321=CARTESIAN_POINT('Ctrl Pts',(-0.375277674973257,0.453180457891261,
-0.65));
#2322=CARTESIAN_POINT('Ctrl Pts',(1.66866520601161E-13,0.561513791224244,
-0.65));
#2323=CARTESIAN_POINT('Ctrl Pts',(0.375277674973257,0.45318045789126,-0.65));
#2324=CARTESIAN_POINT('Ctrl Pts',(-0.750555349946514,0.453180457891261,
-9.19165206894919E-17));
#2325=CARTESIAN_POINT('Ctrl Pts',(-0.562916512459802,0.561513791224244,
-0.325000000000144));
#2326=CARTESIAN_POINT('Ctrl Pts',(-0.375277674973257,0.45318045789126,-0.65));
#2327=CARTESIAN_POINT('Origin',(0.375277674973257,0.,-0.65));
#2328=CARTESIAN_POINT('',(0.375277674973257,0.,-0.65));
#2329=CARTESIAN_POINT('',(0.375277674973257,0.,-0.65));
#2330=CARTESIAN_POINT('',(-0.375277674973257,0.,-0.65));
#2331=CARTESIAN_POINT('',(0.375277674973257,0.,-0.65));
#2332=CARTESIAN_POINT('',(-0.375277674973257,0.,-0.65));
#2333=CARTESIAN_POINT('Origin',(0.750555349946514,0.,0.));
#2334=CARTESIAN_POINT('',(0.750555349946514,0.,0.));
#2335=CARTESIAN_POINT('',(0.750555349946514,0.,0.));
#2336=CARTESIAN_POINT('',(0.750555349946514,0.,0.));
#2337=CARTESIAN_POINT('Origin',(0.375277674973257,0.,0.65));
#2338=CARTESIAN_POINT('',(0.375277674973257,0.,0.65));
#2339=CARTESIAN_POINT('',(0.375277674973257,0.,0.65));
#2340=CARTESIAN_POINT('',(0.375277674973257,0.,0.65));
#2341=CARTESIAN_POINT('Origin',(-0.375277674973257,0.,0.65));
#2342=CARTESIAN_POINT('',(-0.375277674973257,0.,0.65));
#2343=CARTESIAN_POINT('',(-0.375277674973257,0.,0.65));
#2344=CARTESIAN_POINT('',(-0.375277674973257,0.,0.65));
#2345=CARTESIAN_POINT('Origin',(-0.750555349946514,0.,-9.19165206894919E-17));
#2346=CARTESIAN_POINT('',(-0.750555349946514,0.,-9.19165206894919E-17));
#2347=CARTESIAN_POINT('',(-0.750555349946514,0.,-9.19165206894919E-17));
#2348=CARTESIAN_POINT('',(-0.750555349946514,0.,-9.19165206894919E-17));
#2349=CARTESIAN_POINT('Origin',(-0.375277674973257,0.,-0.65));
#2350=CARTESIAN_POINT('',(-0.375277674973257,0.,-0.65));
#2351=CARTESIAN_POINT('Origin',(0.,0.53,-1.11022302462516E-16));
#2352=CARTESIAN_POINT('Origin',(0.,0.,-1.11022302462516E-16));
#2492=UNCERTAINTY_MEASURE_WITH_UNIT(LENGTH_MEASURE(0.001),#2508,
'DISTANCE_ACCURACY_VALUE',
'Maximum model space distance between geometric entities at asserted c
onnectivities');
#2495=UNCERTAINTY_MEASURE_WITH_UNIT(LENGTH_MEASURE(0.001),#2508,
'DISTANCE_ACCURACY_VALUE',
'Maximum model space distance between geometric entities at asserted c
onnectivities');
#2504=(
GEOMETRIC_REPRESENTATION_CONTEXT(3)
GLOBAL_UNCERTAINTY_ASSIGNED_CONTEXT((#2492))
GLOBAL_UNIT_ASSIGNED_CONTEXT((#2508,#2510,#2511))
REPRESENTATION_CONTEXT('','3D')
);
#2507=(
GEOMETRIC_REPRESENTATION_CONTEXT(3)
GLOBAL_UNCERTAINTY_ASSIGNED_CONTEXT((#2495))
GLOBAL_UNIT_ASSIGNED_CONTEXT((#2508,#2510,#2511))
REPRESENTATION_CONTEXT('','3D')
);
#2508=(
LENGTH_UNIT()
NAMED_UNIT(*)
SI_UNIT(.CENTI.,.METRE.)
);
#2510=(
NAMED_UNIT(*)
PLANE_ANGLE_UNIT()
SI_UNIT($,.RADIAN.)
);
#2511=(
NAMED_UNIT(*)
SI_UNIT($,.STERADIAN.)
SOLID_ANGLE_UNIT()
);
#2520=SHAPE_DEFINITION_REPRESENTATION(#2531,#2581);
#2531=PRODUCT_DEFINITION_SHAPE('',$,#2593);
#2581=SHAPE_REPRESENTATION('',(#1562),#2504);
#2584=PRODUCT_DEFINITION_CONTEXT('part definition',#2619,'design');
#2593=PRODUCT_DEFINITION('Hex Bolt - M8x40','Hex Bolt - M8x40',
#2604,#2584);
#2604=PRODUCT_DEFINITION_FORMATION('',$,#2629);
#2619=APPLICATION_CONTEXT(
'Core Data for Automotive Mechanical Design Process');
#2620=PRODUCT_CONTEXT('part definition',#2619,'mechanical');
#2629=PRODUCT('Hex Bolt - M8x40','Hex Bolt - M8x40',
'Hex Bolt - M8x40',(#2620));
#2695=COLOUR_RGB('Black',0.12,0.14,0.17);
#2696=FILL_AREA_STYLE_COLOUR('',#2695);
#2697=FILL_AREA_STYLE('',(#2696));
#2698=SURFACE_STYLE_FILL_AREA(#2697);
#2699=SURFACE_SIDE_STYLE('',(#2698));
#2700=SURFACE_STYLE_USAGE(.BOTH.,#2699);
#2701=PRESENTATION_STYLE_ASSIGNMENT((#2700));
ENDSEC;
END-ISO-10303-21;
